ISO-10303-21;
HEADER;
/* Generated by software containing ST-Developer
 * from STEP Tools, Inc. (www.steptools.com) 
 */

FILE_DESCRIPTION(
/* description */ ('Sub-base valve envelopes and connections'),
/* implementation_level */ '2;1');

FILE_NAME(
/* name */ 'Cap Screw - M4x16.step',
/* time_stamp */ '2026-10-29T15:55:44-07:00',
/* author */ (''),
/* organization */ (''),
/* preprocessor_version */ 'ST-DEVELOPER v20.2',
/* originating_system */ 'Autodesk Translation Framework v15.17.0.0',
/* authorisation */ '');

FILE_SCHEMA (('AUTOMOTIVE_DESIGN { 1 0 10303 214 3 1 1 }'));
ENDSEC;

DATA;
#10=MECHANICAL_DESIGN_GEOMETRIC_PRESENTATION_REPRESENTATION('',(#130),#6113);
#11=ORIENTED_CLOSED_SHELL('',*,#3370,.F.);
#12=BREP_WITH_VOIDS('Body1',#3369,(#11));
#91=CONICAL_SURFACE('',#3865,0.325,0.785398163397448);
#92=CONICAL_SURFACE('',#3869,0.335,0.785398163397448);
#93=CONICAL_SURFACE('',#3873,0.21,0.463647609000806);
#94=CONICAL_SURFACE('',#3877,0.18,0.785398163397448);
#106=SHAPE_REPRESENTATION_RELATIONSHIP('SRR','None',#6181,#118);
#118=ADVANCED_BREP_SHAPE_REPRESENTATION('',(#12),#6112);
#130=STYLED_ITEM('',(#6322),#12);
#258=FACE_BOUND('',#888,.T.);
#375=PLANE('',#3863);
#376=PLANE('',#3871);
#377=PLANE('',#3879);
#378=PLANE('',#3880);
#379=PLANE('',#3881);
#380=PLANE('',#3882);
#381=PLANE('',#3883);
#382=PLANE('',#3884);
#383=PLANE('',#3885);
#384=PLANE('',#3886);
#385=PLANE('',#3887);
#568=FACE_OUTER_BOUND('',#883,.T.);
#569=FACE_OUTER_BOUND('',#884,.T.);
#570=FACE_OUTER_BOUND('',#885,.T.);
#571=FACE_OUTER_BOUND('',#886,.T.);
#572=FACE_OUTER_BOUND('',#887,.T.);
#573=FACE_OUTER_BOUND('',#889,.T.);
#574=FACE_OUTER_BOUND('',#890,.T.);
#575=FACE_OUTER_BOUND('',#891,.T.);
#576=FACE_OUTER_BOUND('',#892,.T.);
#577=FACE_OUTER_BOUND('',#893,.T.);
#578=FACE_OUTER_BOUND('',#894,.T.);
#579=FACE_OUTER_BOUND('',#895,.T.);
#580=FACE_OUTER_BOUND('',#896,.T.);
#581=FACE_OUTER_BOUND('',#897,.T.);
#582=FACE_OUTER_BOUND('',#898,.T.);
#583=FACE_OUTER_BOUND('',#899,.T.);
#584=FACE_OUTER_BOUND('',#900,.T.);
#883=EDGE_LOOP('',(#3011));
#884=EDGE_LOOP('',(#3012,#3013,#3014,#3015));
#885=EDGE_LOOP('',(#3016,#3017,#3018,#3019));
#886=EDGE_LOOP('',(#3020,#3021,#3022,#3023));
#887=EDGE_LOOP('',(#3024));
#888=EDGE_LOOP('',(#3025));
#889=EDGE_LOOP('',(#3026,#3027,#3028,#3029));
#890=EDGE_LOOP('',(#3030,#3031,#3032,#3033));
#891=EDGE_LOOP('',(#3034,#3035,#3036,#3037));
#892=EDGE_LOOP('',(#3038));
#893=EDGE_LOOP('',(#3039,#3040,#3041,#3042));
#894=EDGE_LOOP('',(#3043,#3044,#3045,#3046));
#895=EDGE_LOOP('',(#3047,#3048,#3049,#3050));
#896=EDGE_LOOP('',(#3051,#3052,#3053,#3054));
#897=EDGE_LOOP('',(#3055,#3056,#3057,#3058));
#898=EDGE_LOOP('',(#3059,#3060,#3061,#3062));
#899=EDGE_LOOP('',(#3063,#3064,#3065,#3066,#3067,#3068));
#900=EDGE_LOOP('',(#3069,#3070,#3071,#3072,#3073,#3074));
#1111=LINE('',#6002,#1345);
#1112=LINE('',#6006,#1346);
#1113=LINE('',#6010,#1347);
#1114=LINE('',#6017,#1348);
#1115=LINE('',#6021,#1349);
#1116=LINE('',#6025,#1350);
#1117=LINE('',#6030,#1351);
#1118=LINE('',#6032,#1352);
#1119=LINE('',#6034,#1353);
#1120=LINE('',#6035,#1354);
#1121=LINE('',#6038,#1355);
#1122=LINE('',#6040,#1356);
#1123=LINE('',#6041,#1357);
#1124=LINE('',#6044,#1358);
#1125=LINE('',#6046,#1359);
#1126=LINE('',#6047,#1360);
#1127=LINE('',#6050,#1361);
#1128=LINE('',#6052,#1362);
#1129=LINE('',#6053,#1363);
#1130=LINE('',#6056,#1364);
#1131=LINE('',#6058,#1365);
#1132=LINE('',#6059,#1366);
#1133=LINE('',#6061,#1367);
#1134=LINE('',#6062,#1368);
#1345=VECTOR('',#4841,0.325);
#1346=VECTOR('',#4846,0.35);
#1347=VECTOR('',#4851,0.335);
#1348=VECTOR('',#4860,0.21);
#1349=VECTOR('',#4865,0.2);
#1350=VECTOR('',#4870,0.18);
#1351=VECTOR('',#4875,1.);
#1352=VECTOR('',#4876,1.);
#1353=VECTOR('',#4877,1.);
#1354=VECTOR('',#4878,1.);
#1355=VECTOR('',#4881,1.);
#1356=VECTOR('',#4882,1.);
#1357=VECTOR('',#4883,1.);
#1358=VECTOR('',#4886,1.);
#1359=VECTOR('',#4887,1.);
#1360=VECTOR('',#4888,1.);
#1361=VECTOR('',#4891,1.);
#1362=VECTOR('',#4892,1.);
#1363=VECTOR('',#4893,1.);
#1364=VECTOR('',#4896,1.);
#1365=VECTOR('',#4897,1.);
#1366=VECTOR('',#4898,1.);
#1367=VECTOR('',#4901,1.);
#1368=VECTOR('',#4902,1.);
#1529=CIRCLE('',#3864,0.3);
#1530=CIRCLE('',#3866,0.35);
#1531=CIRCLE('',#3868,0.35);
#1532=CIRCLE('',#3870,0.32);
#1533=CIRCLE('',#3872,0.22);
#1534=CIRCLE('',#3874,0.1954);
#1535=CIRCLE('',#3876,0.1954);
#1536=CIRCLE('',#3878,0.16);
#1795=VERTEX_POINT('',#5997);
#1796=VERTEX_POINT('',#6000);
#1797=VERTEX_POINT('',#6004);
#1798=VERTEX_POINT('',#6008);
#1799=VERTEX_POINT('',#6012);
#1800=VERTEX_POINT('',#6015);
#1801=VERTEX_POINT('',#6019);
#1802=VERTEX_POINT('',#6023);
#1803=VERTEX_POINT('',#6028);
#1804=VERTEX_POINT('',#6029);
#1805=VERTEX_POINT('',#6031);
#1806=VERTEX_POINT('',#6033);
#1807=VERTEX_POINT('',#6037);
#1808=VERTEX_POINT('',#6039);
#1809=VERTEX_POINT('',#6043);
#1810=VERTEX_POINT('',#6045);
#1811=VERTEX_POINT('',#6049);
#1812=VERTEX_POINT('',#6051);
#1813=VERTEX_POINT('',#6055);
#1814=VERTEX_POINT('',#6057);
#2203=EDGE_CURVE('',#1795,#1795,#1529,.T.);
#2204=EDGE_CURVE('',#1796,#1796,#1530,.T.);
#2205=EDGE_CURVE('',#1796,#1795,#1111,.T.);
#2206=EDGE_CURVE('',#1797,#1797,#1531,.T.);
#2207=EDGE_CURVE('',#1797,#1796,#1112,.T.);
#2208=EDGE_CURVE('',#1798,#1798,#1532,.T.);
#2209=EDGE_CURVE('',#1798,#1797,#1113,.T.);
#2210=EDGE_CURVE('',#1799,#1799,#1533,.T.);
#2211=EDGE_CURVE('',#1800,#1800,#1534,.F.);
#2212=EDGE_CURVE('',#1800,#1799,#1114,.T.);
#2213=EDGE_CURVE('',#1801,#1801,#1535,.F.);
#2214=EDGE_CURVE('',#1801,#1800,#1115,.T.);
#2215=EDGE_CURVE('',#1802,#1802,#1536,.T.);
#2216=EDGE_CURVE('',#1802,#1801,#1116,.T.);
#2217=EDGE_CURVE('',#1803,#1804,#1117,.T.);
#2218=EDGE_CURVE('',#1804,#1805,#1118,.T.);
#2219=EDGE_CURVE('',#1805,#1806,#1119,.T.);
#2220=EDGE_CURVE('',#1803,#1806,#1120,.T.);
#2221=EDGE_CURVE('',#1804,#1807,#1121,.T.);
#2222=EDGE_CURVE('',#1807,#1808,#1122,.T.);
#2223=EDGE_CURVE('',#1808,#1805,#1123,.T.);
#2224=EDGE_CURVE('',#1807,#1809,#1124,.T.);
#2225=EDGE_CURVE('',#1809,#1810,#1125,.T.);
#2226=EDGE_CURVE('',#1810,#1808,#1126,.T.);
#2227=EDGE_CURVE('',#1809,#1811,#1127,.T.);
#2228=EDGE_CURVE('',#1811,#1812,#1128,.T.);
#2229=EDGE_CURVE('',#1812,#1810,#1129,.T.);
#2230=EDGE_CURVE('',#1811,#1813,#1130,.T.);
#2231=EDGE_CURVE('',#1813,#1814,#1131,.T.);
#2232=EDGE_CURVE('',#1814,#1812,#1132,.T.);
#2233=EDGE_CURVE('',#1813,#1803,#1133,.T.);
#2234=EDGE_CURVE('',#1806,#1814,#1134,.T.);
#3011=ORIENTED_EDGE('',*,*,#2203,.F.);
#3012=ORIENTED_EDGE('',*,*,#2204,.F.);
#3013=ORIENTED_EDGE('',*,*,#2205,.T.);
#3014=ORIENTED_EDGE('',*,*,#2203,.T.);
#3015=ORIENTED_EDGE('',*,*,#2205,.F.);
#3016=ORIENTED_EDGE('',*,*,#2206,.F.);
#3017=ORIENTED_EDGE('',*,*,#2207,.T.);
#3018=ORIENTED_EDGE('',*,*,#2204,.T.);
#3019=ORIENTED_EDGE('',*,*,#2207,.F.);
#3020=ORIENTED_EDGE('',*,*,#2208,.F.);
#3021=ORIENTED_EDGE('',*,*,#2209,.T.);
#3022=ORIENTED_EDGE('',*,*,#2206,.T.);
#3023=ORIENTED_EDGE('',*,*,#2209,.F.);
#3024=ORIENTED_EDGE('',*,*,#2208,.T.);
#3025=ORIENTED_EDGE('',*,*,#2210,.F.);
#3026=ORIENTED_EDGE('',*,*,#2211,.F.);
#3027=ORIENTED_EDGE('',*,*,#2212,.T.);
#3028=ORIENTED_EDGE('',*,*,#2210,.T.);
#3029=ORIENTED_EDGE('',*,*,#2212,.F.);
#3030=ORIENTED_EDGE('',*,*,#2213,.F.);
#3031=ORIENTED_EDGE('',*,*,#2214,.T.);
#3032=ORIENTED_EDGE('',*,*,#2211,.T.);
#3033=ORIENTED_EDGE('',*,*,#2214,.F.);
#3034=ORIENTED_EDGE('',*,*,#2215,.F.);
#3035=ORIENTED_EDGE('',*,*,#2216,.T.);
#3036=ORIENTED_EDGE('',*,*,#2213,.T.);
#3037=ORIENTED_EDGE('',*,*,#2216,.F.);
#3038=ORIENTED_EDGE('',*,*,#2215,.T.);
#3039=ORIENTED_EDGE('',*,*,#2217,.T.);
#3040=ORIENTED_EDGE('',*,*,#2218,.T.);
#3041=ORIENTED_EDGE('',*,*,#2219,.T.);
#3042=ORIENTED_EDGE('',*,*,#2220,.F.);
#3043=ORIENTED_EDGE('',*,*,#2221,.T.);
#3044=ORIENTED_EDGE('',*,*,#2222,.T.);
#3045=ORIENTED_EDGE('',*,*,#2223,.T.);
#3046=ORIENTED_EDGE('',*,*,#2218,.F.);
#3047=ORIENTED_EDGE('',*,*,#2224,.T.);
#3048=ORIENTED_EDGE('',*,*,#2225,.T.);
#3049=ORIENTED_EDGE('',*,*,#2226,.T.);
#3050=ORIENTED_EDGE('',*,*,#2222,.F.);
#3051=ORIENTED_EDGE('',*,*,#2227,.T.);
#3052=ORIENTED_EDGE('',*,*,#2228,.T.);
#3053=ORIENTED_EDGE('',*,*,#2229,.T.);
#3054=ORIENTED_EDGE('',*,*,#2225,.F.);
#3055=ORIENTED_EDGE('',*,*,#2230,.T.);
#3056=ORIENTED_EDGE('',*,*,#2231,.T.);
#3057=ORIENTED_EDGE('',*,*,#2232,.T.);
#3058=ORIENTED_EDGE('',*,*,#2228,.F.);
#3059=ORIENTED_EDGE('',*,*,#2233,.T.);
#3060=ORIENTED_EDGE('',*,*,#2220,.T.);
#3061=ORIENTED_EDGE('',*,*,#2234,.T.);
#3062=ORIENTED_EDGE('',*,*,#2231,.F.);
#3063=ORIENTED_EDGE('',*,*,#2233,.F.);
#3064=ORIENTED_EDGE('',*,*,#2230,.F.);
#3065=ORIENTED_EDGE('',*,*,#2227,.F.);
#3066=ORIENTED_EDGE('',*,*,#2224,.F.);
#3067=ORIENTED_EDGE('',*,*,#2221,.F.);
#3068=ORIENTED_EDGE('',*,*,#2217,.F.);
#3069=ORIENTED_EDGE('',*,*,#2234,.F.);
#3070=ORIENTED_EDGE('',*,*,#2219,.F.);
#3071=ORIENTED_EDGE('',*,*,#2223,.F.);
#3072=ORIENTED_EDGE('',*,*,#2226,.F.);
#3073=ORIENTED_EDGE('',*,*,#2229,.F.);
#3074=ORIENTED_EDGE('',*,*,#2232,.F.);
#3157=CYLINDRICAL_SURFACE('',#3867,0.35);
#3158=CYLINDRICAL_SURFACE('',#3875,0.1954);
#3341=ADVANCED_FACE('',(#568),#375,.T.);
#3342=ADVANCED_FACE('',(#569),#91,.T.);
#3343=ADVANCED_FACE('',(#570),#3157,.T.);
#3344=ADVANCED_FACE('',(#571),#92,.T.);
#3345=ADVANCED_FACE('',(#572,#258),#376,.T.);
#3346=ADVANCED_FACE('',(#573),#93,.T.);
#3347=ADVANCED_FACE('',(#574),#3158,.T.);
#3348=ADVANCED_FACE('',(#575),#94,.T.);
#3349=ADVANCED_FACE('',(#576),#377,.T.);
#3350=ADVANCED_FACE('',(#577),#378,.F.);
#3351=ADVANCED_FACE('',(#578),#379,.F.);
#3352=ADVANCED_FACE('',(#579),#380,.F.);
#3353=ADVANCED_FACE('',(#580),#381,.F.);
#3354=ADVANCED_FACE('',(#581),#382,.F.);
#3355=ADVANCED_FACE('',(#582),#383,.F.);
#3356=ADVANCED_FACE('',(#583),#384,.F.);
#3357=ADVANCED_FACE('',(#584),#385,.F.);
#3369=CLOSED_SHELL('',(#3341,#3342,#3343,#3344,#3345,#3346,#3347,#3348,
#3349));
#3370=CLOSED_SHELL('',(#3350,#3351,#3352,#3353,#3354,#3355,#3356,#3357));
#3862=AXIS2_PLACEMENT_3D('',#5995,#4831,#4832);
#3863=AXIS2_PLACEMENT_3D('',#5996,#4833,#4834);
#3864=AXIS2_PLACEMENT_3D('',#5998,#4835,#4836);
#3865=AXIS2_PLACEMENT_3D('',#5999,#4837,#4838);
#3866=AXIS2_PLACEMENT_3D('',#6001,#4839,#4840);
#3867=AXIS2_PLACEMENT_3D('',#6003,#4842,#4843);
#3868=AXIS2_PLACEMENT_3D('',#6005,#4844,#4845);
#3869=AXIS2_PLACEMENT_3D('',#6007,#4847,#4848);
#3870=AXIS2_PLACEMENT_3D('',#6009,#4849,#4850);
#3871=AXIS2_PLACEMENT_3D('',#6011,#4852,#4853);
#3872=AXIS2_PLACEMENT_3D('',#6013,#4854,#4855);
#3873=AXIS2_PLACEMENT_3D('',#6014,#4856,#4857);
#3874=AXIS2_PLACEMENT_3D('',#6016,#4858,#4859);
#3875=AXIS2_PLACEMENT_3D('',#6018,#4861,#4862);
#3876=AXIS2_PLACEMENT_3D('',#6020,#4863,#4864);
#3877=AXIS2_PLACEMENT_3D('',#6022,#4866,#4867);
#3878=AXIS2_PLACEMENT_3D('',#6024,#4868,#4869);
#3879=AXIS2_PLACEMENT_3D('',#6026,#4871,#4872);
#3880=AXIS2_PLACEMENT_3D('',#6027,#4873,#4874);
#3881=AXIS2_PLACEMENT_3D('',#6036,#4879,#4880);
#3882=AXIS2_PLACEMENT_3D('',#6042,#4884,#4885);
#3883=AXIS2_PLACEMENT_3D('',#6048,#4889,#4890);
#3884=AXIS2_PLACEMENT_3D('',#6054,#4894,#4895);
#3885=AXIS2_PLACEMENT_3D('',#6060,#4899,#4900);
#3886=AXIS2_PLACEMENT_3D('',#6063,#4903,#4904);
#3887=AXIS2_PLACEMENT_3D('',#6064,#4905,#4906);
#4831=DIRECTION('axis',(0.,0.,1.));
#4832=DIRECTION('refdir',(1.,0.,0.));
#4833=DIRECTION('center_axis',(0.,1.,0.));
#4834=DIRECTION('ref_axis',(0.,0.,1.));
#4835=DIRECTION('center_axis',(0.,-1.,0.));
#4836=DIRECTION('ref_axis',(1.,0.,0.));
#4837=DIRECTION('center_axis',(0.,-1.,0.));
#4838=DIRECTION('ref_axis',(1.,0.,0.));
#4839=DIRECTION('center_axis',(0.,-1.,0.));
#4840=DIRECTION('ref_axis',(1.,0.,0.));
#4841=DIRECTION('',(0.707106781186547,0.707106781186548,8.65956056235493E-17));
#4842=DIRECTION('center_axis',(0.,-1.,0.));
#4843=DIRECTION('ref_axis',(1.,0.,0.));
#4844=DIRECTION('center_axis',(0.,-1.,0.));
#4845=DIRECTION('ref_axis',(1.,0.,0.));
#4846=DIRECTION('',(0.,1.,0.));
#4847=DIRECTION('center_axis',(0.,1.,0.));
#4848=DIRECTION('ref_axis',(1.,0.,0.));
#4849=DIRECTION('center_axis',(0.,-1.,0.));
#4850=DIRECTION('ref_axis',(1.,0.,0.));
#4851=DIRECTION('',(-0.707106781186547,0.707106781186548,-8.65956056235493E-17));
#4852=DIRECTION('center_axis',(0.,-1.,0.));
#4853=DIRECTION('ref_axis',(0.,0.,-1.));
#4854=DIRECTION('center_axis',(0.,-1.,0.));
#4855=DIRECTION('ref_axis',(1.,0.,0.));
#4856=DIRECTION('center_axis',(0.,1.,0.));
#4857=DIRECTION('ref_axis',(1.,0.,0.));
#4858=DIRECTION('center_axis',(0.,1.,0.));
#4859=DIRECTION('ref_axis',(1.,0.,0.));
#4860=DIRECTION('',(-0.447213595499958,0.894427190999916,-5.47678698264203E-17));
#4861=DIRECTION('center_axis',(0.,-1.,0.));
#4862=DIRECTION('ref_axis',(1.,0.,0.));
#4863=DIRECTION('center_axis',(0.,1.,0.));
#4864=DIRECTION('ref_axis',(1.,0.,0.));
#4865=DIRECTION('',(0.,1.,0.));
#4866=DIRECTION('center_axis',(0.,1.,0.));
#4867=DIRECTION('ref_axis',(1.,0.,0.));
#4868=DIRECTION('center_axis',(0.,-1.,0.));
#4869=DIRECTION('ref_axis',(1.,0.,0.));
#4870=DIRECTION('',(-0.707106781186547,0.707106781186548,-8.65956056235493E-17));
#4871=DIRECTION('center_axis',(0.,-1.,0.));
#4872=DIRECTION('ref_axis',(0.,0.,-1.));
#4873=DIRECTION('center_axis',(0.866025403784439,0.,-0.5));
#4874=DIRECTION('ref_axis',(0.5,0.,0.866025403784439));
#4875=DIRECTION('',(-0.5,0.,-0.866025403784439));
#4876=DIRECTION('',(0.,-1.,0.));
#4877=DIRECTION('',(0.5,0.,0.866025403784439));
#4878=DIRECTION('',(0.,-1.,0.));
#4879=DIRECTION('center_axis',(1.60246890531964E-16,0.,-1.));
#4880=DIRECTION('ref_axis',(1.,0.,1.60246890531964E-16));
#4881=DIRECTION('',(-1.,0.,-1.60246890531964E-16));
#4882=DIRECTION('',(0.,-1.,0.));
#4883=DIRECTION('',(1.,0.,1.60246890531964E-16));
#4884=DIRECTION('center_axis',(-0.866025403784439,0.,-0.5));
#4885=DIRECTION('ref_axis',(0.5,0.,-0.866025403784439));
#4886=DIRECTION('',(-0.5,0.,0.866025403784439));
#4887=DIRECTION('',(0.,-1.,0.));
#4888=DIRECTION('',(0.5,0.,-0.866025403784439));
#4889=DIRECTION('center_axis',(-0.866025403784439,0.,0.5));
#4890=DIRECTION('ref_axis',(-0.5,0.,-0.866025403784439));
#4891=DIRECTION('',(0.5,0.,0.866025403784439));
#4892=DIRECTION('',(0.,-1.,0.));
#4893=DIRECTION('',(-0.5,0.,-0.866025403784439));
#4894=DIRECTION('center_axis',(-1.60246890531964E-16,0.,1.));
#4895=DIRECTION('ref_axis',(-1.,0.,-1.60246890531964E-16));
#4896=DIRECTION('',(1.,0.,1.60246890531964E-16));
#4897=DIRECTION('',(0.,-1.,0.));
#4898=DIRECTION('',(-1.,0.,-1.60246890531964E-16));
#4899=DIRECTION('center_axis',(0.866025403784439,0.,0.5));
#4900=DIRECTION('ref_axis',(-0.5,0.,0.866025403784439));
#4901=DIRECTION('',(0.5,0.,-0.866025403784439));
#4902=DIRECTION('',(-0.5,0.,0.866025403784439));
#4903=DIRECTION('center_axis',(0.,1.,0.));
#4904=DIRECTION('ref_axis',(1.,0.,0.));
#4905=DIRECTION('center_axis',(0.,-1.,0.));
#4906=DIRECTION('ref_axis',(0.,0.,-1.));
#5995=CARTESIAN_POINT('',(0.,0.,0.));
#5996=CARTESIAN_POINT('Origin',(0.3,0.4,0.));
#5997=CARTESIAN_POINT('',(-0.3,0.4,-3.67394039744206E-17));
#5998=CARTESIAN_POINT('Origin',(0.,0.4,0.));
#5999=CARTESIAN_POINT('Origin',(0.,0.375,0.));
#6000=CARTESIAN_POINT('',(-0.35,0.35,-4.28626379701573E-17));
#6001=CARTESIAN_POINT('Origin',(0.,0.35,0.));
#6002=CARTESIAN_POINT('',(-0.325,0.375,-3.9801020972289E-17));
#6003=CARTESIAN_POINT('Origin',(0.,0.19,0.));
#6004=CARTESIAN_POINT('',(-0.35,0.03,-4.28626379701574E-17));
#6005=CARTESIAN_POINT('Origin',(0.,0.03,0.));
#6006=CARTESIAN_POINT('',(-0.35,0.19,-4.28626379701574E-17));
#6007=CARTESIAN_POINT('Origin',(0.,0.0149999999999999,0.));
#6008=CARTESIAN_POINT('',(-0.32,-3.29597460435593E-17,-3.91886975727153E-17));
#6009=CARTESIAN_POINT('Origin',(0.,0.,0.));
#6010=CARTESIAN_POINT('',(-0.335,0.0149999999999999,-4.10256677714363E-17));
#6011=CARTESIAN_POINT('Origin',(0.22,0.,0.));
#6012=CARTESIAN_POINT('',(-0.22,-6.93889390390723E-18,-2.69422295812418E-17));
#6013=CARTESIAN_POINT('Origin',(0.,0.,0.));
#6014=CARTESIAN_POINT('Origin',(0.,-0.02,0.));
#6015=CARTESIAN_POINT('',(-0.1954,-0.0492,2.39295984553393E-17));
#6016=CARTESIAN_POINT('Origin',(0.,-0.0492,0.));
#6017=CARTESIAN_POINT('',(-0.21,-0.02,-2.57175827820944E-17));
#6018=CARTESIAN_POINT('Origin',(0.,-0.8,0.));
#6019=CARTESIAN_POINT('',(-0.1954,-1.5646,2.39295984553393E-17));
#6020=CARTESIAN_POINT('Origin',(0.,-1.5646,0.));
#6021=CARTESIAN_POINT('',(-0.1954,-0.8,-2.39295984553393E-17));
#6022=CARTESIAN_POINT('Origin',(0.,-1.58,0.));
#6023=CARTESIAN_POINT('',(-0.16,-1.6,-1.95943487863577E-17));
#6024=CARTESIAN_POINT('Origin',(0.,-1.6,0.));
#6025=CARTESIAN_POINT('',(-0.18,-1.58,-2.20436423846524E-17));
#6026=CARTESIAN_POINT('Origin',(0.,-1.6,0.));
#6027=CARTESIAN_POINT('Origin',(0.0866025403784439,-0.4,-0.15));
#6028=CARTESIAN_POINT('',(0.173205080756888,-0.4,0.));
#6029=CARTESIAN_POINT('',(0.0866025403784439,-0.4,-0.15));
#6030=CARTESIAN_POINT('',(0.173205080756888,-0.4,0.));
#6031=CARTESIAN_POINT('',(0.0866025403784439,-0.64,-0.15));
#6032=CARTESIAN_POINT('',(0.0866025403784439,-0.4,-0.15));
#6033=CARTESIAN_POINT('',(0.173205080756888,-0.64,0.));
#6034=CARTESIAN_POINT('',(0.173205080756888,-0.64,0.));
#6035=CARTESIAN_POINT('',(0.173205080756888,-0.4,0.));
#6036=CARTESIAN_POINT('Origin',(-0.0866025403784438,-0.4,-0.15));
#6037=CARTESIAN_POINT('',(-0.0866025403784438,-0.4,-0.15));
#6038=CARTESIAN_POINT('',(0.0866025403784439,-0.4,-0.15));
#6039=CARTESIAN_POINT('',(-0.0866025403784438,-0.64,-0.15));
#6040=CARTESIAN_POINT('',(-0.0866025403784438,-0.4,-0.15));
#6041=CARTESIAN_POINT('',(0.0866025403784439,-0.64,-0.15));
#6042=CARTESIAN_POINT('Origin',(-0.173205080756888,-0.4,-2.77555756156289E-17));
#6043=CARTESIAN_POINT('',(-0.173205080756888,-0.4,-2.12115047744981E-17));
#6044=CARTESIAN_POINT('',(-0.0866025403784438,-0.4,-0.15));
#6045=CARTESIAN_POINT('',(-0.173205080756888,-0.64,-2.77555756156289E-17));
#6046=CARTESIAN_POINT('',(-0.173205080756888,-0.4,-2.12115047744981E-17));
#6047=CARTESIAN_POINT('',(-0.0866025403784438,-0.64,-0.15));
#6048=CARTESIAN_POINT('Origin',(-0.0866025403784439,-0.4,0.15));
#6049=CARTESIAN_POINT('',(-0.0866025403784439,-0.4,0.15));
#6050=CARTESIAN_POINT('',(-0.173205080756888,-0.4,-2.12115047744981E-17));
#6051=CARTESIAN_POINT('',(-0.0866025403784439,-0.64,0.15));
#6052=CARTESIAN_POINT('',(-0.0866025403784439,-0.4,0.15));
#6053=CARTESIAN_POINT('',(-0.173205080756888,-0.64,-2.12115047744981E-17));
#6054=CARTESIAN_POINT('Origin',(0.0866025403784439,-0.4,0.15));
#6055=CARTESIAN_POINT('',(0.0866025403784439,-0.4,0.15));
#6056=CARTESIAN_POINT('',(-0.0866025403784439,-0.4,0.15));
#6057=CARTESIAN_POINT('',(0.0866025403784439,-0.64,0.15));
#6058=CARTESIAN_POINT('',(0.0866025403784439,-0.4,0.15));
#6059=CARTESIAN_POINT('',(-0.0866025403784439,-0.64,0.15));
#6060=CARTESIAN_POINT('Origin',(0.173205080756888,-0.4,0.));
#6061=CARTESIAN_POINT('',(0.0866025403784439,-0.4,0.15));
#6062=CARTESIAN_POINT('',(0.0866025403784439,-0.64,0.15));
#6063=CARTESIAN_POINT('Origin',(0.,-0.4,-2.77555756156289E-17));
#6064=CARTESIAN_POINT('Origin',(0.,-0.64,-2.77555756156289E-17));
#6096=UNCERTAINTY_MEASURE_WITH_UNIT(LENGTH_MEASURE(0.001),#6114,
'DISTANCE_ACCURACY_VALUE',
'Maximum model space distance between geometric entities at asserted c
onnectivities');
#6097=UNCERTAINTY_MEASURE_WITH_UNIT(LENGTH_MEASURE(0.001),#6114,
'DISTANCE_ACCURACY_VALUE',
'Maximum model space distance between geometric entities at asserted c
onnectivities');
#6112=(
GEOMETRIC_REPRESENTATION_CONTEXT(3)
GLOBAL_UNCERTAINTY_ASSIGNED_CONTEXT((#6096))
GLOBAL_UNIT_ASSIGNED_CONTEXT((#6114,#6116,#6117))
REPRESENTATION_CONTEXT('','3D')
);
#6113=(
GEOMETRIC_REPRESENTATION_CONTEXT(3)
GLOBAL_UNCERTAINTY_ASSIGNED_CONTEXT((#6097))
GLOBAL_UNIT_ASSIGNED_CONTEXT((#6114,#6116,#6117))
REPRESENTATION_CONTEXT('','3D')
);
#6114=(
LENGTH_UNIT()
NAMED_UNIT(*)
SI_UNIT(.CENTI.,.METRE.)
);
#6116=(
NAMED_UNIT(*)
PLANE_ANGLE_UNIT()
SI_UNIT($,.RADIAN.)
);
#6117=(
NAMED_UNIT(*)
SI_UNIT($,.STERADIAN.)
SOLID_ANGLE_UNIT()
);
#6132=SHAPE_DEFINITION_REPRESENTATION(#6149,#6181);
#6149=PRODUCT_DEFINITION_SHAPE('',$,#6197);
#6181=SHAPE_REPRESENTATION('',(#3862),#6112);
#6182=PRODUCT_DEFINITION_CONTEXT('part definition',#6229,'design');
#6197=PRODUCT_DEFINITION('Cap Screw - M4x16',
'Cap Screw - M4x16',#6212,#6182);
#6212=PRODUCT_DEFINITION_FORMATION('',$,#6245);
#6229=APPLICATION_CONTEXT(
'Core Data for Automotive Mechanical Design Process');
#6230=PRODUCT_CONTEXT('part definition',#6229,'mechanical');
#6245=PRODUCT('Cap Screw - M4x16','Cap Screw - M4x16',
'Cap Screw - M4x16',(#6230));
#6316=COLOUR_RGB('Black',0.12,0.14,0.17);
#6317=FILL_AREA_STYLE_COLOUR('',#6316);
#6318=FILL_AREA_STYLE('',(#6317));
#6319=SURFACE_STYLE_FILL_AREA(#6318);
#6320=SURFACE_SIDE_STYLE('',(#6319));
#6321=SURFACE_STYLE_USAGE(.BOTH.,#6320);
#6322=PRESENTATION_STYLE_ASSIGNMENT((#6321));
ENDSEC;
END-ISO-10303-21;
